ISO-10303-21;
HEADER;
/* Generated by software containing ST-Developer
 * from STEP Tools, Inc. (www.steptools.com) 
 */

FILE_DESCRIPTION(
/* description */ ('Hand-crank flanged shaft unit'),
/* implementation_level */ '2;1');

FILE_NAME(
/* name */ 'Flange bolt sleeve (7).step',
/* time_stamp */ '2026-10-27T18:35:45-07:00',
/* author */ (''),
/* organization */ (''),
/* preprocessor_version */ 'ST-DEVELOPER v20.2',
/* originating_system */ 'Autodesk Translation Framework v15.17.0.0',
/* authorisation */ '');

FILE_SCHEMA (('AUTOMOTIVE_DESIGN { 1 0 10303 214 3 1 1 }'));
ENDSEC;

DATA;
#10=MECHANICAL_DESIGN_GEOMETRIC_PRESENTATION_REPRESENTATION('',(#287),#6805);
#247=SHAPE_REPRESENTATION_RELATIONSHIP('SRR','None',#6908,#267);
#267=ADVANCED_BREP_SHAPE_REPRESENTATION('',(#308),#6791);
#287=STYLED_ITEM('',(#7098),#308);
#308=MANIFOLD_SOLID_BREP('Body1',#3328);
#356=FACE_BOUND('',#796,.T.);
#357=FACE_BOUND('',#798,.T.);
#440=PLANE('',#3671);
#441=PLANE('',#3672);
#569=FACE_OUTER_BOUND('',#793,.T.);
#570=FACE_OUTER_BOUND('',#794,.T.);
#571=FACE_OUTER_BOUND('',#795,.T.);
#572=FACE_OUTER_BOUND('',#797,.T.);
#793=EDGE_LOOP('',(#2467,#2468,#2469,#2470));
#794=EDGE_LOOP('',(#2471,#2472,#2473,#2474));
#795=EDGE_LOOP('',(#2475));
#796=EDGE_LOOP('',(#2476));
#797=EDGE_LOOP('',(#2477));
#798=EDGE_LOOP('',(#2478));
#1041=LINE('',#5181,#1269);
#1042=LINE('',#5187,#1270);
#1269=VECTOR('',#4226,0.425);
#1270=VECTOR('',#4233,0.595);
#1485=CIRCLE('',#3666,0.425);
#1486=CIRCLE('',#3667,0.425);
#1487=CIRCLE('',#3669,0.595);
#1488=CIRCLE('',#3670,0.595);
#1641=VERTEX_POINT('',#5178);
#1642=VERTEX_POINT('',#5180);
#1643=VERTEX_POINT('',#5184);
#1644=VERTEX_POINT('',#5186);
#1951=EDGE_CURVE('',#1641,#1641,#1485,.T.);
#1952=EDGE_CURVE('',#1641,#1642,#1041,.T.);
#1953=EDGE_CURVE('',#1642,#1642,#1486,.T.);
#1954=EDGE_CURVE('',#1643,#1643,#1487,.T.);
#1955=EDGE_CURVE('',#1643,#1644,#1042,.T.);
#1956=EDGE_CURVE('',#1644,#1644,#1488,.T.);
#2467=ORIENTED_EDGE('',*,*,#1951,.F.);
#2468=ORIENTED_EDGE('',*,*,#1952,.T.);
#2469=ORIENTED_EDGE('',*,*,#1953,.T.);
#2470=ORIENTED_EDGE('',*,*,#1952,.F.);
#2471=ORIENTED_EDGE('',*,*,#1954,.F.);
#2472=ORIENTED_EDGE('',*,*,#1955,.T.);
#2473=ORIENTED_EDGE('',*,*,#1956,.T.);
#2474=ORIENTED_EDGE('',*,*,#1955,.F.);
#2475=ORIENTED_EDGE('',*,*,#1954,.T.);
#2476=ORIENTED_EDGE('',*,*,#1951,.T.);
#2477=ORIENTED_EDGE('',*,*,#1956,.F.);
#2478=ORIENTED_EDGE('',*,*,#1953,.F.);
#3091=CYLINDRICAL_SURFACE('',#3665,0.425);
#3092=CYLINDRICAL_SURFACE('',#3668,0.595);
#3186=ADVANCED_FACE('',(#569),#3091,.F.);
#3187=ADVANCED_FACE('',(#570),#3092,.T.);
#3188=ADVANCED_FACE('',(#571,#356),#440,.T.);
#3189=ADVANCED_FACE('',(#572,#357),#441,.F.);
#3328=CLOSED_SHELL('',(#3186,#3187,#3188,#3189));
#3664=AXIS2_PLACEMENT_3D('',#5176,#4220,#4221);
#3665=AXIS2_PLACEMENT_3D('',#5177,#4222,#4223);
#3666=AXIS2_PLACEMENT_3D('',#5179,#4224,#4225);
#3667=AXIS2_PLACEMENT_3D('',#5182,#4227,#4228);
#3668=AXIS2_PLACEMENT_3D('',#5183,#4229,#4230);
#3669=AXIS2_PLACEMENT_3D('',#5185,#4231,#4232);
#3670=AXIS2_PLACEMENT_3D('',#5188,#4234,#4235);
#3671=AXIS2_PLACEMENT_3D('',#5189,#4236,#4237);
#3672=AXIS2_PLACEMENT_3D('',#5190,#4238,#4239);
#4220=DIRECTION('axis',(0.,0.,1.));
#4221=DIRECTION('refdir',(1.,0.,0.));
#4222=DIRECTION('center_axis',(0.,1.,0.));
#4223=DIRECTION('ref_axis',(1.,0.,0.));
#4224=DIRECTION('center_axis',(0.,-1.,0.));
#4225=DIRECTION('ref_axis',(1.,0.,0.));
#4226=DIRECTION('',(0.,-1.,0.));
#4227=DIRECTION('center_axis',(0.,-1.,0.));
#4228=DIRECTION('ref_axis',(1.,0.,0.));
#4229=DIRECTION('center_axis',(0.,1.,0.));
#4230=DIRECTION('ref_axis',(1.,0.,0.));
#4231=DIRECTION('center_axis',(0.,1.,0.));
#4232=DIRECTION('ref_axis',(1.,0.,0.));
#4233=DIRECTION('',(0.,-1.,0.));
#4234=DIRECTION('center_axis',(0.,1.,0.));
#4235=DIRECTION('ref_axis',(1.,0.,0.));
#4236=DIRECTION('center_axis',(0.,1.,0.));
#4237=DIRECTION('ref_axis',(1.,0.,0.));
#4238=DIRECTION('center_axis',(0.,1.,0.));
#4239=DIRECTION('ref_axis',(1.,0.,0.));
#5176=CARTESIAN_POINT('',(0.,0.,0.));
#5177=CARTESIAN_POINT('Origin',(3.2,21.,10.7));
#5178=CARTESIAN_POINT('',(2.775,22.,10.7));
#5179=CARTESIAN_POINT('Origin',(3.2,22.,10.7));
#5180=CARTESIAN_POINT('',(2.775,21.,10.7));
#5181=CARTESIAN_POINT('',(2.775,21.,10.7));
#5182=CARTESIAN_POINT('Origin',(3.2,21.,10.7));
#5183=CARTESIAN_POINT('Origin',(3.2,21.,10.7));
#5184=CARTESIAN_POINT('',(2.605,22.,10.7));
#5185=CARTESIAN_POINT('Origin',(3.2,22.,10.7));
#5186=CARTESIAN_POINT('',(2.605,21.,10.7));
#5187=CARTESIAN_POINT('',(2.605,21.,10.7));
#5188=CARTESIAN_POINT('Origin',(3.2,21.,10.7));
#5189=CARTESIAN_POINT('Origin',(3.2,22.,10.7));
#5190=CARTESIAN_POINT('Origin',(3.2,21.,10.7));
#6766=UNCERTAINTY_MEASURE_WITH_UNIT(LENGTH_MEASURE(0.001),#6806,
'DISTANCE_ACCURACY_VALUE',
'Maximum model space distance between geometric entities at asserted c
onnectivities');
#6780=UNCERTAINTY_MEASURE_WITH_UNIT(LENGTH_MEASURE(0.001),#6806,
'DISTANCE_ACCURACY_VALUE',
'Maximum model space distance between geometric entities at asserted c
onnectivities');
#6791=(
GEOMETRIC_REPRESENTATION_CONTEXT(3)
GLOBAL_UNCERTAINTY_ASSIGNED_CONTEXT((#6766))
GLOBAL_UNIT_ASSIGNED_CONTEXT((#6806,#6808,#6809))
REPRESENTATION_CONTEXT('','3D')
);
#6805=(
GEOMETRIC_REPRESENTATION_CONTEXT(3)
GLOBAL_UNCERTAINTY_ASSIGNED_CONTEXT((#6780))
GLOBAL_UNIT_ASSIGNED_CONTEXT((#6806,#6808,#6809))
REPRESENTATION_CONTEXT('','3D')
);
#6806=(
LENGTH_UNIT()
NAMED_UNIT(*)
SI_UNIT(.CENTI.,.METRE.)
);
#6808=(
NAMED_UNIT(*)
PLANE_ANGLE_UNIT()
SI_UNIT($,.RADIAN.)
);
#6809=(
NAMED_UNIT(*)
SI_UNIT($,.STERADIAN.)
SOLID_ANGLE_UNIT()
);
#6820=SHAPE_DEFINITION_REPRESENTATION(#6844,#6908);
#6844=PRODUCT_DEFINITION_SHAPE('',$,#6933);
#6908=SHAPE_REPRESENTATION('',(#3664),#6791);
#6922=PRODUCT_DEFINITION_CONTEXT('part definition',#6996,'design');
#6933=PRODUCT_DEFINITION('Flange bolt sleeve (7)',
'Flange bolt sleeve (7)',#6957,#6922);
#6957=PRODUCT_DEFINITION_FORMATION('',$,#7008);
#6996=APPLICATION_CONTEXT(
'Core Data for Automotive Mechanical Design Process');
#6997=PRODUCT_CONTEXT('part definition',#6996,'mechanical');
#7008=PRODUCT('Flange bolt sleeve (7)','Flange bolt sleeve (7)',
'Flange bolt sleeve (7)',(#6997));
#7092=COLOUR_RGB('Black',0.12,0.14,0.17);
#7093=FILL_AREA_STYLE_COLOUR('',#7092);
#7094=FILL_AREA_STYLE('',(#7093));
#7095=SURFACE_STYLE_FILL_AREA(#7094);
#7096=SURFACE_SIDE_STYLE('',(#7095));
#7097=SURFACE_STYLE_USAGE(.BOTH.,#7096);
#7098=PRESENTATION_STYLE_ASSIGNMENT((#7097));
ENDSEC;
END-ISO-10303-21;
